ISO-10303-21;
HEADER;
/* Generated by software containing ST-Developer
 * from STEP Tools, Inc. (www.steptools.com) 
 */

FILE_DESCRIPTION(
/* description */ ('Double-row support with tensioned shaft'),
/* implementation_level */ '2;1');

FILE_NAME(
/* name */ 'Flange hole reducer (2).step',
/* time_stamp */ '2026-10-27T10:50:35-07:00',
/* author */ (''),
/* organization */ (''),
/* preprocessor_version */ 'ST-DEVELOPER v20.2',
/* originating_system */ 'Autodesk Translation Framework v15.17.0.0',
/* authorisation */ '');

FILE_SCHEMA (('AUTOMOTIVE_DESIGN { 1 0 10303 214 3 1 1 }'));
ENDSEC;

DATA;
#10=MECHANICAL_DESIGN_GEOMETRIC_PRESENTATION_REPRESENTATION('',(#487),#11559);
#423=SHAPE_REPRESENTATION_RELATIONSHIP('SRR','None',#11731,#455);
#455=ADVANCED_BREP_SHAPE_REPRESENTATION('',(#520),#11533);
#487=STYLED_ITEM('',(#11981),#520);
#520=MANIFOLD_SOLID_BREP('Body1',#6332);
#584=FACE_BOUND('',#1371,.T.);
#585=FACE_BOUND('',#1373,.T.);
#721=PLANE('',#6841);
#722=PLANE('',#6842);
#982=FACE_OUTER_BOUND('',#1368,.T.);
#983=FACE_OUTER_BOUND('',#1369,.T.);
#984=FACE_OUTER_BOUND('',#1370,.T.);
#985=FACE_OUTER_BOUND('',#1372,.T.);
#1368=EDGE_LOOP('',(#4624,#4625,#4626,#4627));
#1369=EDGE_LOOP('',(#4628,#4629,#4630,#4631));
#1370=EDGE_LOOP('',(#4632));
#1371=EDGE_LOOP('',(#4633));
#1372=EDGE_LOOP('',(#4634));
#1373=EDGE_LOOP('',(#4635));
#1843=LINE('',#9559,#2390);
#1844=LINE('',#9565,#2391);
#2390=VECTOR('',#7720,0.425);
#2391=VECTOR('',#7727,0.595);
#2882=CIRCLE('',#6836,0.425);
#2883=CIRCLE('',#6837,0.425);
#2884=CIRCLE('',#6839,0.595);
#2885=CIRCLE('',#6840,0.595);
#3125=VERTEX_POINT('',#9556);
#3126=VERTEX_POINT('',#9558);
#3127=VERTEX_POINT('',#9562);
#3128=VERTEX_POINT('',#9564);
#3697=EDGE_CURVE('',#3125,#3125,#2882,.T.);
#3698=EDGE_CURVE('',#3125,#3126,#1843,.T.);
#3699=EDGE_CURVE('',#3126,#3126,#2883,.T.);
#3700=EDGE_CURVE('',#3127,#3127,#2884,.T.);
#3701=EDGE_CURVE('',#3127,#3128,#1844,.T.);
#3702=EDGE_CURVE('',#3128,#3128,#2885,.T.);
#4624=ORIENTED_EDGE('',*,*,#3697,.F.);
#4625=ORIENTED_EDGE('',*,*,#3698,.T.);
#4626=ORIENTED_EDGE('',*,*,#3699,.T.);
#4627=ORIENTED_EDGE('',*,*,#3698,.F.);
#4628=ORIENTED_EDGE('',*,*,#3700,.F.);
#4629=ORIENTED_EDGE('',*,*,#3701,.T.);
#4630=ORIENTED_EDGE('',*,*,#3702,.T.);
#4631=ORIENTED_EDGE('',*,*,#3701,.F.);
#4632=ORIENTED_EDGE('',*,*,#3700,.T.);
#4633=ORIENTED_EDGE('',*,*,#3697,.T.);
#4634=ORIENTED_EDGE('',*,*,#3702,.F.);
#4635=ORIENTED_EDGE('',*,*,#3699,.F.);
#5913=CYLINDRICAL_SURFACE('',#6835,0.425);
#5914=CYLINDRICAL_SURFACE('',#6838,0.595);
#6045=ADVANCED_FACE('',(#982),#5913,.F.);
#6046=ADVANCED_FACE('',(#983),#5914,.T.);
#6047=ADVANCED_FACE('',(#984,#584),#721,.T.);
#6048=ADVANCED_FACE('',(#985,#585),#722,.F.);
#6332=CLOSED_SHELL('',(#6045,#6046,#6047,#6048));
#6834=AXIS2_PLACEMENT_3D('',#9554,#7714,#7715);
#6835=AXIS2_PLACEMENT_3D('',#9555,#7716,#7717);
#6836=AXIS2_PLACEMENT_3D('',#9557,#7718,#7719);
#6837=AXIS2_PLACEMENT_3D('',#9560,#7721,#7722);
#6838=AXIS2_PLACEMENT_3D('',#9561,#7723,#7724);
#6839=AXIS2_PLACEMENT_3D('',#9563,#7725,#7726);
#6840=AXIS2_PLACEMENT_3D('',#9566,#7728,#7729);
#6841=AXIS2_PLACEMENT_3D('',#9567,#7730,#7731);
#6842=AXIS2_PLACEMENT_3D('',#9568,#7732,#7733);
#7714=DIRECTION('axis',(0.,0.,1.));
#7715=DIRECTION('refdir',(1.,0.,0.));
#7716=DIRECTION('center_axis',(0.,1.,0.));
#7717=DIRECTION('ref_axis',(1.,0.,0.));
#7718=DIRECTION('center_axis',(0.,-1.,0.));
#7719=DIRECTION('ref_axis',(1.,0.,0.));
#7720=DIRECTION('',(0.,-1.,0.));
#7721=DIRECTION('center_axis',(0.,-1.,0.));
#7722=DIRECTION('ref_axis',(1.,0.,0.));
#7723=DIRECTION('center_axis',(0.,1.,0.));
#7724=DIRECTION('ref_axis',(1.,0.,0.));
#7725=DIRECTION('center_axis',(0.,1.,0.));
#7726=DIRECTION('ref_axis',(1.,0.,0.));
#7727=DIRECTION('',(0.,-1.,0.));
#7728=DIRECTION('center_axis',(0.,1.,0.));
#7729=DIRECTION('ref_axis',(1.,0.,0.));
#7730=DIRECTION('center_axis',(0.,1.,0.));
#7731=DIRECTION('ref_axis',(1.,0.,0.));
#7732=DIRECTION('center_axis',(0.,1.,0.));
#7733=DIRECTION('ref_axis',(1.,0.,0.));
#9554=CARTESIAN_POINT('',(0.,0.,0.));
#9555=CARTESIAN_POINT('Origin',(3.2,-0.5,6.8));
#9556=CARTESIAN_POINT('',(2.775,0.5,6.8));
#9557=CARTESIAN_POINT('Origin',(3.2,0.5,6.8));
#9558=CARTESIAN_POINT('',(2.775,-0.5,6.8));
#9559=CARTESIAN_POINT('',(2.775,-0.5,6.8));
#9560=CARTESIAN_POINT('Origin',(3.2,-0.5,6.8));
#9561=CARTESIAN_POINT('Origin',(3.2,-0.5,6.8));
#9562=CARTESIAN_POINT('',(2.605,0.5,6.8));
#9563=CARTESIAN_POINT('Origin',(3.2,0.5,6.8));
#9564=CARTESIAN_POINT('',(2.605,-0.5,6.8));
#9565=CARTESIAN_POINT('',(2.605,-0.5,6.8));
#9566=CARTESIAN_POINT('Origin',(3.2,-0.5,6.8));
#9567=CARTESIAN_POINT('Origin',(3.2,0.5,6.8));
#9568=CARTESIAN_POINT('Origin',(3.2,-0.5,6.8));
#11496=UNCERTAINTY_MEASURE_WITH_UNIT(LENGTH_MEASURE(0.001),#11560,
'DISTANCE_ACCURACY_VALUE',
'Maximum model space distance between geometric entities at asserted c
onnectivities');
#11522=UNCERTAINTY_MEASURE_WITH_UNIT(LENGTH_MEASURE(0.001),#11560,
'DISTANCE_ACCURACY_VALUE',
'Maximum model space distance between geometric entities at asserted c
onnectivities');
#11533=(
GEOMETRIC_REPRESENTATION_CONTEXT(3)
GLOBAL_UNCERTAINTY_ASSIGNED_CONTEXT((#11496))
GLOBAL_UNIT_ASSIGNED_CONTEXT((#11560,#11562,#11563))
REPRESENTATION_CONTEXT('','3D')
);
#11559=(
GEOMETRIC_REPRESENTATION_CONTEXT(3)
GLOBAL_UNCERTAINTY_ASSIGNED_CONTEXT((#11522))
GLOBAL_UNIT_ASSIGNED_CONTEXT((#11560,#11562,#11563))
REPRESENTATION_CONTEXT('','3D')
);
#11560=(
LENGTH_UNIT()
NAMED_UNIT(*)
SI_UNIT(.CENTI.,.METRE.)
);
#11562=(
NAMED_UNIT(*)
PLANE_ANGLE_UNIT()
SI_UNIT($,.RADIAN.)
);
#11563=(
NAMED_UNIT(*)
SI_UNIT($,.STERADIAN.)
SOLID_ANGLE_UNIT()
);
#11574=SHAPE_DEFINITION_REPRESENTATION(#11610,#11731);
#11610=PRODUCT_DEFINITION_SHAPE('',$,#11768);
#11731=SHAPE_REPRESENTATION('',(#6834),#11533);
#11757=PRODUCT_DEFINITION_CONTEXT('part definition',#11867,'design');
#11768=PRODUCT_DEFINITION('Flange hole reducer (2)',
'Flange hole reducer (2)',#11804,#11757);
#11804=PRODUCT_DEFINITION_FORMATION('',$,#11879);
#11867=APPLICATION_CONTEXT(
'Core Data for Automotive Mechanical Design Process');
#11868=PRODUCT_CONTEXT('part definition',#11867,'mechanical');
#11879=PRODUCT('Flange hole reducer (2)','Flange hole reducer (2)',
'Flange hole reducer (2)',(#11868));
#11975=COLOUR_RGB('Off White',0.89,0.88,0.83);
#11976=FILL_AREA_STYLE_COLOUR('',#11975);
#11977=FILL_AREA_STYLE('',(#11976));
#11978=SURFACE_STYLE_FILL_AREA(#11977);
#11979=SURFACE_SIDE_STYLE('',(#11978));
#11980=SURFACE_STYLE_USAGE(.BOTH.,#11979);
#11981=PRESENTATION_STYLE_ASSIGNMENT((#11980));
ENDSEC;
END-ISO-10303-21;
